ISO-10303-21;
HEADER;
/* Generated by software containing ST-Developer
 * from STEP Tools, Inc. (www.steptools.com) 
 */

FILE_DESCRIPTION(
/* description */ ('Self-centering screw clamp'),
/* implementation_level */ '2;1');

FILE_NAME(
/* name */ 'M4x10 Cap Screw.step',
/* time_stamp */ '2026-10-28T03:25:31-07:00',
/* author */ (''),
/* organization */ (''),
/* preprocessor_version */ 'ST-DEVELOPER v20.2',
/* originating_system */ 'Autodesk Translation Framework v15.17.0.0',
/* authorisation */ '');

FILE_SCHEMA (('AUTOMOTIVE_DESIGN { 1 0 10303 214 3 1 1 }'));
ENDSEC;

DATA;
#10=MECHANICAL_DESIGN_GEOMETRIC_PRESENTATION_REPRESENTATION('',(#662),#16799);
#11=ORIENTED_CLOSED_SHELL('',*,#9113,.F.);
#13=BREP_WITH_VOIDS('Body1',#9114,(#11));
#489=CONICAL_SURFACE('',#10493,0.325,0.785398163397448);
#490=CONICAL_SURFACE('',#10497,0.335,0.785398163397448);
#491=CONICAL_SURFACE('',#10501,0.21,0.463647609000806);
#573=SHAPE_REPRESENTATION_RELATIONSHIP('SRR','None',#17050,#614);
#614=ADVANCED_BREP_SHAPE_REPRESENTATION('',(#13),#16788);
#662=STYLED_ITEM('',(#17333),#13);
#992=FACE_BOUND('',#2477,.T.);
#1217=PLANE('',#10481);
#1218=PLANE('',#10482);
#1219=PLANE('',#10483);
#1220=PLANE('',#10484);
#1221=PLANE('',#10485);
#1222=PLANE('',#10486);
#1223=PLANE('',#10487);
#1224=PLANE('',#10488);
#1225=PLANE('',#10489);
#1226=PLANE('',#10491);
#1227=PLANE('',#10499);
#1685=FACE_OUTER_BOUND('',#2463,.T.);
#1686=FACE_OUTER_BOUND('',#2464,.T.);
#1687=FACE_OUTER_BOUND('',#2465,.T.);
#1688=FACE_OUTER_BOUND('',#2466,.T.);
#1689=FACE_OUTER_BOUND('',#2467,.T.);
#1690=FACE_OUTER_BOUND('',#2468,.T.);
#1691=FACE_OUTER_BOUND('',#2469,.T.);
#1692=FACE_OUTER_BOUND('',#2470,.T.);
#1693=FACE_OUTER_BOUND('',#2471,.T.);
#1694=FACE_OUTER_BOUND('',#2472,.T.);
#1695=FACE_OUTER_BOUND('',#2473,.T.);
#1696=FACE_OUTER_BOUND('',#2474,.T.);
#1697=FACE_OUTER_BOUND('',#2475,.T.);
#1698=FACE_OUTER_BOUND('',#2476,.T.);
#1699=FACE_OUTER_BOUND('',#2478,.T.);
#1700=FACE_OUTER_BOUND('',#2479,.T.);
#2463=EDGE_LOOP('',(#8007,#8008,#8009,#8010));
#2464=EDGE_LOOP('',(#8011,#8012,#8013,#8014));
#2465=EDGE_LOOP('',(#8015,#8016,#8017,#8018));
#2466=EDGE_LOOP('',(#8019,#8020,#8021,#8022));
#2467=EDGE_LOOP('',(#8023,#8024,#8025,#8026));
#2468=EDGE_LOOP('',(#8027,#8028,#8029,#8030));
#2469=EDGE_LOOP('',(#8031,#8032,#8033,#8034,#8035,#8036));
#2470=EDGE_LOOP('',(#8037,#8038,#8039,#8040,#8041,#8042));
#2471=EDGE_LOOP('',(#8043));
#2472=EDGE_LOOP('',(#8044));
#2473=EDGE_LOOP('',(#8045,#8046,#8047,#8048));
#2474=EDGE_LOOP('',(#8049,#8050,#8051,#8052));
#2475=EDGE_LOOP('',(#8053,#8054,#8055,#8056));
#2476=EDGE_LOOP('',(#8057));
#2477=EDGE_LOOP('',(#8058));
#2478=EDGE_LOOP('',(#8059,#8060,#8061,#8062));
#2479=EDGE_LOOP('',(#8063,#8064,#8065,#8066));
#3052=LINE('',#16091,#3625);
#3053=LINE('',#16093,#3626);
#3054=LINE('',#16095,#3627);
#3055=LINE('',#16096,#3628);
#3056=LINE('',#16099,#3629);
#3057=LINE('',#16101,#3630);
#3058=LINE('',#16102,#3631);
#3059=LINE('',#16105,#3632);
#3060=LINE('',#16107,#3633);
#3061=LINE('',#16108,#3634);
#3062=LINE('',#16111,#3635);
#3063=LINE('',#16113,#3636);
#3064=LINE('',#16114,#3637);
#3065=LINE('',#16117,#3638);
#3066=LINE('',#16119,#3639);
#3067=LINE('',#16120,#3640);
#3068=LINE('',#16122,#3641);
#3069=LINE('',#16123,#3642);
#3070=LINE('',#16135,#3643);
#3071=LINE('',#16139,#3644);
#3072=LINE('',#16143,#3645);
#3073=LINE('',#16150,#3646);
#3074=LINE('',#16152,#3647);
#3625=VECTOR('',#13037,1.);
#3626=VECTOR('',#13038,1.);
#3627=VECTOR('',#13039,1.);
#3628=VECTOR('',#13040,1.);
#3629=VECTOR('',#13043,1.);
#3630=VECTOR('',#13044,1.);
#3631=VECTOR('',#13045,1.);
#3632=VECTOR('',#13048,1.);
#3633=VECTOR('',#13049,1.);
#3634=VECTOR('',#13050,1.);
#3635=VECTOR('',#13053,1.);
#3636=VECTOR('',#13054,1.);
#3637=VECTOR('',#13055,1.);
#3638=VECTOR('',#13058,1.);
#3639=VECTOR('',#13059,1.);
#3640=VECTOR('',#13060,1.);
#3641=VECTOR('',#13063,1.);
#3642=VECTOR('',#13064,1.);
#3643=VECTOR('',#13081,0.325);
#3644=VECTOR('',#13086,0.35);
#3645=VECTOR('',#13091,0.335);
#3646=VECTOR('',#13100,0.21);
#3647=VECTOR('',#13103,0.2);
#4170=CIRCLE('',#10490,0.1954);
#4171=CIRCLE('',#10492,0.3);
#4172=CIRCLE('',#10494,0.35);
#4173=CIRCLE('',#10496,0.35);
#4174=CIRCLE('',#10498,0.32);
#4175=CIRCLE('',#10500,0.22);
#4176=CIRCLE('',#10502,0.1954);
#4863=VERTEX_POINT('',#16089);
#4864=VERTEX_POINT('',#16090);
#4865=VERTEX_POINT('',#16092);
#4866=VERTEX_POINT('',#16094);
#4867=VERTEX_POINT('',#16098);
#4868=VERTEX_POINT('',#16100);
#4869=VERTEX_POINT('',#16104);
#4870=VERTEX_POINT('',#16106);
#4871=VERTEX_POINT('',#16110);
#4872=VERTEX_POINT('',#16112);
#4873=VERTEX_POINT('',#16116);
#4874=VERTEX_POINT('',#16118);
#4875=VERTEX_POINT('',#16127);
#4876=VERTEX_POINT('',#16130);
#4877=VERTEX_POINT('',#16133);
#4878=VERTEX_POINT('',#16137);
#4879=VERTEX_POINT('',#16141);
#4880=VERTEX_POINT('',#16145);
#4881=VERTEX_POINT('',#16148);
#5928=EDGE_CURVE('',#4863,#4864,#3052,.T.);
#5929=EDGE_CURVE('',#4864,#4865,#3053,.T.);
#5930=EDGE_CURVE('',#4865,#4866,#3054,.T.);
#5931=EDGE_CURVE('',#4863,#4866,#3055,.T.);
#5932=EDGE_CURVE('',#4864,#4867,#3056,.T.);
#5933=EDGE_CURVE('',#4867,#4868,#3057,.T.);
#5934=EDGE_CURVE('',#4868,#4865,#3058,.T.);
#5935=EDGE_CURVE('',#4867,#4869,#3059,.T.);
#5936=EDGE_CURVE('',#4869,#4870,#3060,.T.);
#5937=EDGE_CURVE('',#4870,#4868,#3061,.T.);
#5938=EDGE_CURVE('',#4869,#4871,#3062,.T.);
#5939=EDGE_CURVE('',#4871,#4872,#3063,.T.);
#5940=EDGE_CURVE('',#4872,#4870,#3064,.T.);
#5941=EDGE_CURVE('',#4871,#4873,#3065,.T.);
#5942=EDGE_CURVE('',#4873,#4874,#3066,.T.);
#5943=EDGE_CURVE('',#4874,#4872,#3067,.T.);
#5944=EDGE_CURVE('',#4873,#4863,#3068,.T.);
#5945=EDGE_CURVE('',#4866,#4874,#3069,.T.);
#5946=EDGE_CURVE('',#4875,#4875,#4170,.T.);
#5947=EDGE_CURVE('',#4876,#4876,#4171,.T.);
#5948=EDGE_CURVE('',#4877,#4877,#4172,.T.);
#5949=EDGE_CURVE('',#4877,#4876,#3070,.T.);
#5950=EDGE_CURVE('',#4878,#4878,#4173,.T.);
#5951=EDGE_CURVE('',#4878,#4877,#3071,.T.);
#5952=EDGE_CURVE('',#4879,#4879,#4174,.T.);
#5953=EDGE_CURVE('',#4879,#4878,#3072,.T.);
#5954=EDGE_CURVE('',#4880,#4880,#4175,.T.);
#5955=EDGE_CURVE('',#4881,#4881,#4176,.F.);
#5956=EDGE_CURVE('',#4881,#4880,#3073,.T.);
#5957=EDGE_CURVE('',#4875,#4881,#3074,.T.);
#8007=ORIENTED_EDGE('',*,*,#5928,.T.);
#8008=ORIENTED_EDGE('',*,*,#5929,.T.);
#8009=ORIENTED_EDGE('',*,*,#5930,.T.);
#8010=ORIENTED_EDGE('',*,*,#5931,.F.);
#8011=ORIENTED_EDGE('',*,*,#5932,.T.);
#8012=ORIENTED_EDGE('',*,*,#5933,.T.);
#8013=ORIENTED_EDGE('',*,*,#5934,.T.);
#8014=ORIENTED_EDGE('',*,*,#5929,.F.);
#8015=ORIENTED_EDGE('',*,*,#5935,.T.);
#8016=ORIENTED_EDGE('',*,*,#5936,.T.);
#8017=ORIENTED_EDGE('',*,*,#5937,.T.);
#8018=ORIENTED_EDGE('',*,*,#5933,.F.);
#8019=ORIENTED_EDGE('',*,*,#5938,.T.);
#8020=ORIENTED_EDGE('',*,*,#5939,.T.);
#8021=ORIENTED_EDGE('',*,*,#5940,.T.);
#8022=ORIENTED_EDGE('',*,*,#5936,.F.);
#8023=ORIENTED_EDGE('',*,*,#5941,.T.);
#8024=ORIENTED_EDGE('',*,*,#5942,.T.);
#8025=ORIENTED_EDGE('',*,*,#5943,.T.);
#8026=ORIENTED_EDGE('',*,*,#5939,.F.);
#8027=ORIENTED_EDGE('',*,*,#5944,.T.);
#8028=ORIENTED_EDGE('',*,*,#5931,.T.);
#8029=ORIENTED_EDGE('',*,*,#5945,.T.);
#8030=ORIENTED_EDGE('',*,*,#5942,.F.);
#8031=ORIENTED_EDGE('',*,*,#5944,.F.);
#8032=ORIENTED_EDGE('',*,*,#5941,.F.);
#8033=ORIENTED_EDGE('',*,*,#5938,.F.);
#8034=ORIENTED_EDGE('',*,*,#5935,.F.);
#8035=ORIENTED_EDGE('',*,*,#5932,.F.);
#8036=ORIENTED_EDGE('',*,*,#5928,.F.);
#8037=ORIENTED_EDGE('',*,*,#5945,.F.);
#8038=ORIENTED_EDGE('',*,*,#5930,.F.);
#8039=ORIENTED_EDGE('',*,*,#5934,.F.);
#8040=ORIENTED_EDGE('',*,*,#5937,.F.);
#8041=ORIENTED_EDGE('',*,*,#5940,.F.);
#8042=ORIENTED_EDGE('',*,*,#5943,.F.);
#8043=ORIENTED_EDGE('',*,*,#5946,.F.);
#8044=ORIENTED_EDGE('',*,*,#5947,.F.);
#8045=ORIENTED_EDGE('',*,*,#5948,.F.);
#8046=ORIENTED_EDGE('',*,*,#5949,.T.);
#8047=ORIENTED_EDGE('',*,*,#5947,.T.);
#8048=ORIENTED_EDGE('',*,*,#5949,.F.);
#8049=ORIENTED_EDGE('',*,*,#5950,.F.);
#8050=ORIENTED_EDGE('',*,*,#5951,.T.);
#8051=ORIENTED_EDGE('',*,*,#5948,.T.);
#8052=ORIENTED_EDGE('',*,*,#5951,.F.);
#8053=ORIENTED_EDGE('',*,*,#5952,.F.);
#8054=ORIENTED_EDGE('',*,*,#5953,.T.);
#8055=ORIENTED_EDGE('',*,*,#5950,.T.);
#8056=ORIENTED_EDGE('',*,*,#5953,.F.);
#8057=ORIENTED_EDGE('',*,*,#5952,.T.);
#8058=ORIENTED_EDGE('',*,*,#5954,.F.);
#8059=ORIENTED_EDGE('',*,*,#5955,.F.);
#8060=ORIENTED_EDGE('',*,*,#5956,.T.);
#8061=ORIENTED_EDGE('',*,*,#5954,.T.);
#8062=ORIENTED_EDGE('',*,*,#5956,.F.);
#8063=ORIENTED_EDGE('',*,*,#5946,.T.);
#8064=ORIENTED_EDGE('',*,*,#5957,.T.);
#8065=ORIENTED_EDGE('',*,*,#5955,.T.);
#8066=ORIENTED_EDGE('',*,*,#5957,.F.);
#8544=CYLINDRICAL_SURFACE('',#10495,0.35);
#8545=CYLINDRICAL_SURFACE('',#10503,0.1954);
#8983=ADVANCED_FACE('',(#1685),#1217,.F.);
#8984=ADVANCED_FACE('',(#1686),#1218,.F.);
#8985=ADVANCED_FACE('',(#1687),#1219,.F.);
#8986=ADVANCED_FACE('',(#1688),#1220,.F.);
#8987=ADVANCED_FACE('',(#1689),#1221,.F.);
#8988=ADVANCED_FACE('',(#1690),#1222,.F.);
#8989=ADVANCED_FACE('',(#1691),#1223,.F.);
#8990=ADVANCED_FACE('',(#1692),#1224,.F.);
#8991=ADVANCED_FACE('',(#1693),#1225,.F.);
#8992=ADVANCED_FACE('',(#1694),#1226,.T.);
#8993=ADVANCED_FACE('',(#1695),#489,.T.);
#8994=ADVANCED_FACE('',(#1696),#8544,.T.);
#8995=ADVANCED_FACE('',(#1697),#490,.T.);
#8996=ADVANCED_FACE('',(#1698,#992),#1227,.T.);
#8997=ADVANCED_FACE('',(#1699),#491,.T.);
#8998=ADVANCED_FACE('',(#1700),#8545,.T.);
#9113=CLOSED_SHELL('',(#8983,#8984,#8985,#8986,#8987,#8988,#8989,#8990));
#9114=CLOSED_SHELL('',(#8991,#8992,#8993,#8994,#8995,#8996,#8997,#8998));
#10480=AXIS2_PLACEMENT_3D('',#16087,#13033,#13034);
#10481=AXIS2_PLACEMENT_3D('',#16088,#13035,#13036);
#10482=AXIS2_PLACEMENT_3D('',#16097,#13041,#13042);
#10483=AXIS2_PLACEMENT_3D('',#16103,#13046,#13047);
#10484=AXIS2_PLACEMENT_3D('',#16109,#13051,#13052);
#10485=AXIS2_PLACEMENT_3D('',#16115,#13056,#13057);
#10486=AXIS2_PLACEMENT_3D('',#16121,#13061,#13062);
#10487=AXIS2_PLACEMENT_3D('',#16124,#13065,#13066);
#10488=AXIS2_PLACEMENT_3D('',#16125,#13067,#13068);
#10489=AXIS2_PLACEMENT_3D('',#16126,#13069,#13070);
#10490=AXIS2_PLACEMENT_3D('',#16128,#13071,#13072);
#10491=AXIS2_PLACEMENT_3D('',#16129,#13073,#13074);
#10492=AXIS2_PLACEMENT_3D('',#16131,#13075,#13076);
#10493=AXIS2_PLACEMENT_3D('',#16132,#13077,#13078);
#10494=AXIS2_PLACEMENT_3D('',#16134,#13079,#13080);
#10495=AXIS2_PLACEMENT_3D('',#16136,#13082,#13083);
#10496=AXIS2_PLACEMENT_3D('',#16138,#13084,#13085);
#10497=AXIS2_PLACEMENT_3D('',#16140,#13087,#13088);
#10498=AXIS2_PLACEMENT_3D('',#16142,#13089,#13090);
#10499=AXIS2_PLACEMENT_3D('',#16144,#13092,#13093);
#10500=AXIS2_PLACEMENT_3D('',#16146,#13094,#13095);
#10501=AXIS2_PLACEMENT_3D('',#16147,#13096,#13097);
#10502=AXIS2_PLACEMENT_3D('',#16149,#13098,#13099);
#10503=AXIS2_PLACEMENT_3D('',#16151,#13101,#13102);
#13033=DIRECTION('axis',(0.,0.,1.));
#13034=DIRECTION('refdir',(1.,0.,0.));
#13035=DIRECTION('center_axis',(0.866025403784439,0.,-0.5));
#13036=DIRECTION('ref_axis',(0.5,0.,0.866025403784439));
#13037=DIRECTION('',(-0.5,0.,-0.866025403784439));
#13038=DIRECTION('',(0.,-1.,0.));
#13039=DIRECTION('',(0.5,0.,0.866025403784439));
#13040=DIRECTION('',(0.,-1.,0.));
#13041=DIRECTION('center_axis',(1.60246890531964E-16,0.,-1.));
#13042=DIRECTION('ref_axis',(1.,0.,1.60246890531964E-16));
#13043=DIRECTION('',(-1.,0.,-1.60246890531964E-16));
#13044=DIRECTION('',(0.,-1.,0.));
#13045=DIRECTION('',(1.,0.,1.60246890531964E-16));
#13046=DIRECTION('center_axis',(-0.866025403784439,0.,-0.5));
#13047=DIRECTION('ref_axis',(0.5,0.,-0.866025403784439));
#13048=DIRECTION('',(-0.5,0.,0.866025403784439));
#13049=DIRECTION('',(0.,-1.,0.));
#13050=DIRECTION('',(0.5,0.,-0.866025403784439));
#13051=DIRECTION('center_axis',(-0.866025403784439,0.,0.5));
#13052=DIRECTION('ref_axis',(-0.5,0.,-0.866025403784439));
#13053=DIRECTION('',(0.5,0.,0.866025403784439));
#13054=DIRECTION('',(0.,-1.,0.));
#13055=DIRECTION('',(-0.5,0.,-0.866025403784439));
#13056=DIRECTION('center_axis',(-1.60246890531964E-16,0.,1.));
#13057=DIRECTION('ref_axis',(-1.,0.,-1.60246890531964E-16));
#13058=DIRECTION('',(1.,0.,1.60246890531964E-16));
#13059=DIRECTION('',(0.,-1.,0.));
#13060=DIRECTION('',(-1.,0.,-1.60246890531964E-16));
#13061=DIRECTION('center_axis',(0.866025403784439,0.,0.5));
#13062=DIRECTION('ref_axis',(-0.5,0.,0.866025403784439));
#13063=DIRECTION('',(0.5,0.,-0.866025403784439));
#13064=DIRECTION('',(-0.5,0.,0.866025403784439));
#13065=DIRECTION('center_axis',(0.,1.,0.));
#13066=DIRECTION('ref_axis',(1.,0.,0.));
#13067=DIRECTION('center_axis',(0.,-1.,0.));
#13068=DIRECTION('ref_axis',(0.,0.,-1.));
#13069=DIRECTION('center_axis',(0.,1.,0.));
#13070=DIRECTION('ref_axis',(1.,0.,0.));
#13071=DIRECTION('center_axis',(0.,1.,0.));
#13072=DIRECTION('ref_axis',(1.,0.,0.));
#13073=DIRECTION('center_axis',(0.,1.,0.));
#13074=DIRECTION('ref_axis',(0.,0.,1.));
#13075=DIRECTION('center_axis',(0.,-1.,0.));
#13076=DIRECTION('ref_axis',(1.,0.,0.));
#13077=DIRECTION('center_axis',(0.,-1.,0.));
#13078=DIRECTION('ref_axis',(1.,0.,0.));
#13079=DIRECTION('center_axis',(0.,-1.,0.));
#13080=DIRECTION('ref_axis',(1.,0.,0.));
#13081=DIRECTION('',(0.707106781186547,0.707106781186548,8.65956056235493E-17));
#13082=DIRECTION('center_axis',(0.,-1.,0.));
#13083=DIRECTION('ref_axis',(1.,0.,0.));
#13084=DIRECTION('center_axis',(0.,-1.,0.));
#13085=DIRECTION('ref_axis',(1.,0.,0.));
#13086=DIRECTION('',(0.,1.,0.));
#13087=DIRECTION('center_axis',(0.,1.,0.));
#13088=DIRECTION('ref_axis',(1.,0.,0.));
#13089=DIRECTION('center_axis',(0.,-1.,0.));
#13090=DIRECTION('ref_axis',(1.,0.,0.));
#13091=DIRECTION('',(-0.707106781186547,0.707106781186548,-8.65956056235493E-17));
#13092=DIRECTION('center_axis',(0.,-1.,0.));
#13093=DIRECTION('ref_axis',(0.,0.,-1.));
#13094=DIRECTION('center_axis',(0.,-1.,0.));
#13095=DIRECTION('ref_axis',(1.,0.,0.));
#13096=DIRECTION('center_axis',(0.,1.,0.));
#13097=DIRECTION('ref_axis',(1.,0.,0.));
#13098=DIRECTION('center_axis',(0.,1.,0.));
#13099=DIRECTION('ref_axis',(1.,0.,0.));
#13100=DIRECTION('',(-0.447213595499958,0.894427190999916,-5.47678698264203E-17));
#13101=DIRECTION('center_axis',(0.,-1.,0.));
#13102=DIRECTION('ref_axis',(1.,0.,0.));
#13103=DIRECTION('',(0.,1.,0.));
#16087=CARTESIAN_POINT('',(0.,0.,0.));
#16088=CARTESIAN_POINT('Origin',(0.0866025403784439,-0.4,-0.15));
#16089=CARTESIAN_POINT('',(0.173205080756888,-0.4,0.));
#16090=CARTESIAN_POINT('',(0.0866025403784439,-0.4,-0.15));
#16091=CARTESIAN_POINT('',(0.173205080756888,-0.4,0.));
#16092=CARTESIAN_POINT('',(0.0866025403784439,-0.64,-0.15));
#16093=CARTESIAN_POINT('',(0.0866025403784439,-0.4,-0.15));
#16094=CARTESIAN_POINT('',(0.173205080756888,-0.64,0.));
#16095=CARTESIAN_POINT('',(0.173205080756888,-0.64,0.));
#16096=CARTESIAN_POINT('',(0.173205080756888,-0.4,0.));
#16097=CARTESIAN_POINT('Origin',(-0.0866025403784438,-0.4,-0.15));
#16098=CARTESIAN_POINT('',(-0.0866025403784438,-0.4,-0.15));
#16099=CARTESIAN_POINT('',(0.0866025403784439,-0.4,-0.15));
#16100=CARTESIAN_POINT('',(-0.0866025403784438,-0.64,-0.15));
#16101=CARTESIAN_POINT('',(-0.0866025403784438,-0.4,-0.15));
#16102=CARTESIAN_POINT('',(0.0866025403784439,-0.64,-0.15));
#16103=CARTESIAN_POINT('Origin',(-0.173205080756888,-0.4,-2.77555756156289E-17));
#16104=CARTESIAN_POINT('',(-0.173205080756888,-0.4,-2.12115047744981E-17));
#16105=CARTESIAN_POINT('',(-0.0866025403784438,-0.4,-0.15));
#16106=CARTESIAN_POINT('',(-0.173205080756888,-0.64,-2.77555756156289E-17));
#16107=CARTESIAN_POINT('',(-0.173205080756888,-0.4,-2.12115047744981E-17));
#16108=CARTESIAN_POINT('',(-0.0866025403784438,-0.64,-0.15));
#16109=CARTESIAN_POINT('Origin',(-0.0866025403784439,-0.4,0.15));
#16110=CARTESIAN_POINT('',(-0.0866025403784439,-0.4,0.15));
#16111=CARTESIAN_POINT('',(-0.173205080756888,-0.4,-2.12115047744981E-17));
#16112=CARTESIAN_POINT('',(-0.0866025403784439,-0.64,0.15));
#16113=CARTESIAN_POINT('',(-0.0866025403784439,-0.4,0.15));
#16114=CARTESIAN_POINT('',(-0.173205080756888,-0.64,-2.12115047744981E-17));
#16115=CARTESIAN_POINT('Origin',(0.0866025403784439,-0.4,0.15));
#16116=CARTESIAN_POINT('',(0.0866025403784439,-0.4,0.15));
#16117=CARTESIAN_POINT('',(-0.0866025403784439,-0.4,0.15));
#16118=CARTESIAN_POINT('',(0.0866025403784439,-0.64,0.15));
#16119=CARTESIAN_POINT('',(0.0866025403784439,-0.4,0.15));
#16120=CARTESIAN_POINT('',(-0.0866025403784439,-0.64,0.15));
#16121=CARTESIAN_POINT('Origin',(0.173205080756888,-0.4,0.));
#16122=CARTESIAN_POINT('',(0.0866025403784439,-0.4,0.15));
#16123=CARTESIAN_POINT('',(0.0866025403784439,-0.64,0.15));
#16124=CARTESIAN_POINT('Origin',(0.,-0.4,-2.77555756156289E-17));
#16125=CARTESIAN_POINT('Origin',(0.,-0.64,-2.77555756156289E-17));
#16126=CARTESIAN_POINT('Origin',(0.,-1.,0.));
#16127=CARTESIAN_POINT('',(-0.1954,-1.,2.39295984553393E-17));
#16128=CARTESIAN_POINT('Origin',(0.,-1.,0.));
#16129=CARTESIAN_POINT('Origin',(0.3,0.4,0.));
#16130=CARTESIAN_POINT('',(-0.3,0.4,-3.67394039744206E-17));
#16131=CARTESIAN_POINT('Origin',(0.,0.4,0.));
#16132=CARTESIAN_POINT('Origin',(0.,0.375,0.));
#16133=CARTESIAN_POINT('',(-0.35,0.35,-4.28626379701573E-17));
#16134=CARTESIAN_POINT('Origin',(0.,0.35,0.));
#16135=CARTESIAN_POINT('',(-0.325,0.375,-3.9801020972289E-17));
#16136=CARTESIAN_POINT('Origin',(0.,0.19,0.));
#16137=CARTESIAN_POINT('',(-0.35,0.03,-4.28626379701574E-17));
#16138=CARTESIAN_POINT('Origin',(0.,0.03,0.));
#16139=CARTESIAN_POINT('',(-0.35,0.19,-4.28626379701574E-17));
#16140=CARTESIAN_POINT('Origin',(0.,0.0149999999999999,0.));
#16141=CARTESIAN_POINT('',(-0.32,-3.29597460435593E-17,-3.91886975727153E-17));
#16142=CARTESIAN_POINT('Origin',(0.,0.,0.));
#16143=CARTESIAN_POINT('',(-0.335,0.0149999999999999,-4.10256677714363E-17));
#16144=CARTESIAN_POINT('Origin',(0.22,0.,0.));
#16145=CARTESIAN_POINT('',(-0.22,-6.93889390390723E-18,-2.69422295812418E-17));
#16146=CARTESIAN_POINT('Origin',(0.,0.,0.));
#16147=CARTESIAN_POINT('Origin',(0.,-0.02,0.));
#16148=CARTESIAN_POINT('',(-0.1954,-0.0492,2.39295984553393E-17));
#16149=CARTESIAN_POINT('Origin',(0.,-0.0492,0.));
#16150=CARTESIAN_POINT('',(-0.21,-0.02,-2.57175827820944E-17));
#16151=CARTESIAN_POINT('Origin',(0.,-0.8,0.));
#16152=CARTESIAN_POINT('',(-0.1954,-0.8,-2.39295984553393E-17));
#16739=UNCERTAINTY_MEASURE_WITH_UNIT(LENGTH_MEASURE(0.001),#16800,
'DISTANCE_ACCURACY_VALUE',
'Maximum model space distance between geometric entities at asserted c
onnectivities');
#16750=UNCERTAINTY_MEASURE_WITH_UNIT(LENGTH_MEASURE(0.001),#16800,
'DISTANCE_ACCURACY_VALUE',
'Maximum model space distance between geometric entities at asserted c
onnectivities');
#16788=(
GEOMETRIC_REPRESENTATION_CONTEXT(3)
GLOBAL_UNCERTAINTY_ASSIGNED_CONTEXT((#16739))
GLOBAL_UNIT_ASSIGNED_CONTEXT((#16800,#16802,#16803))
REPRESENTATION_CONTEXT('','3D')
);
#16799=(
GEOMETRIC_REPRESENTATION_CONTEXT(3)
GLOBAL_UNCERTAINTY_ASSIGNED_CONTEXT((#16750))
GLOBAL_UNIT_ASSIGNED_CONTEXT((#16800,#16802,#16803))
REPRESENTATION_CONTEXT('','3D')
);
#16800=(
LENGTH_UNIT()
NAMED_UNIT(*)
SI_UNIT(.CENTI.,.METRE.)
);
#16802=(
NAMED_UNIT(*)
PLANE_ANGLE_UNIT()
SI_UNIT($,.RADIAN.)
);
#16803=(
NAMED_UNIT(*)
SI_UNIT($,.STERADIAN.)
SOLID_ANGLE_UNIT()
);
#16841=SHAPE_DEFINITION_REPRESENTATION(#16896,#17050);
#16896=PRODUCT_DEFINITION_SHAPE('',$,#17099);
#17050=SHAPE_REPRESENTATION('',(#10480),#16788);
#17061=PRODUCT_DEFINITION_CONTEXT('part definition',#17207,'design');
#17099=PRODUCT_DEFINITION('M4x10 Cap Screw','M4x10 Cap Screw',#17147,#17061);
#17147=PRODUCT_DEFINITION_FORMATION('',$,#17246);
#17207=APPLICATION_CONTEXT(
'Core Data for Automotive Mechanical Design Process');
#17208=PRODUCT_CONTEXT('part definition',#17207,'mechanical');
#17246=PRODUCT('M4x10 Cap Screw','M4x10 Cap Screw','M4x10 Cap Screw',(#17208));
#17327=COLOUR_RGB('Black',0.12,0.14,0.17);
#17328=FILL_AREA_STYLE_COLOUR('',#17327);
#17329=FILL_AREA_STYLE('',(#17328));
#17330=SURFACE_STYLE_FILL_AREA(#17329);
#17331=SURFACE_SIDE_STYLE('',(#17330));
#17332=SURFACE_STYLE_USAGE(.BOTH.,#17331);
#17333=PRESENTATION_STYLE_ASSIGNMENT((#17332));
ENDSEC;
END-ISO-10303-21;
